ISO-10303-21;
HEADER;
/* Generated by software containing ST-Developer
 * from STEP Tools, Inc. (www.steptools.com) 
 */

FILE_DESCRIPTION(
/* description */ ('Chain-less indexing wheel (Geneva) drive'),
/* implementation_level */ '2;1');

FILE_NAME(
/* name */ 'Bearing cap (1).step',
/* time_stamp */ '2026-10-28T03:25:22-07:00',
/* author */ (''),
/* organization */ (''),
/* preprocessor_version */ 'ST-DEVELOPER v20.2',
/* originating_system */ 'Autodesk Translation Framework v15.17.0.0',
/* authorisation */ '');

FILE_SCHEMA (('AUTOMOTIVE_DESIGN { 1 0 10303 214 3 1 1 }'));
ENDSEC;

DATA;
#10=MECHANICAL_DESIGN_GEOMETRIC_PRESENTATION_REPRESENTATION('',(#308),#10957);
#258=SHAPE_REPRESENTATION_RELATIONSHIP('SRR','None',#11071,#283);
#283=ADVANCED_BREP_SHAPE_REPRESENTATION('',(#341),#10934);
#308=STYLED_ITEM('',(#11287),#341);
#341=MANIFOLD_SOLID_BREP('Body1',#5704);
#412=FACE_BOUND('',#1122,.T.);
#413=FACE_BOUND('',#1124,.T.);
#414=FACE_BOUND('',#1127,.T.);
#415=FACE_BOUND('',#1130,.T.);
#416=FACE_BOUND('',#1133,.T.);
#417=FACE_BOUND('',#1140,.T.);
#418=FACE_BOUND('',#1144,.T.);
#419=FACE_BOUND('',#1145,.T.);
#420=FACE_BOUND('',#1146,.T.);
#421=FACE_BOUND('',#1147,.T.);
#422=FACE_BOUND('',#1148,.T.);
#521=PLANE('',#6199);
#522=PLANE('',#6203);
#523=PLANE('',#6209);
#524=PLANE('',#6215);
#525=PLANE('',#6221);
#526=PLANE('',#6238);
#527=PLANE('',#6243);
#742=FACE_OUTER_BOUND('',#1120,.T.);
#743=FACE_OUTER_BOUND('',#1121,.T.);
#744=FACE_OUTER_BOUND('',#1123,.T.);
#745=FACE_OUTER_BOUND('',#1125,.T.);
#746=FACE_OUTER_BOUND('',#1126,.T.);
#747=FACE_OUTER_BOUND('',#1128,.T.);
#748=FACE_OUTER_BOUND('',#1129,.T.);
#749=FACE_OUTER_BOUND('',#1131,.T.);
#750=FACE_OUTER_BOUND('',#1132,.T.);
#751=FACE_OUTER_BOUND('',#1134,.T.);
#752=FACE_OUTER_BOUND('',#1135,.T.);
#753=FACE_OUTER_BOUND('',#1136,.T.);
#754=FACE_OUTER_BOUND('',#1137,.T.);
#755=FACE_OUTER_BOUND('',#1138,.T.);
#756=FACE_OUTER_BOUND('',#1139,.T.);
#757=FACE_OUTER_BOUND('',#1141,.T.);
#758=FACE_OUTER_BOUND('',#1142,.T.);
#759=FACE_OUTER_BOUND('',#1143,.T.);
#1120=EDGE_LOOP('',(#4145,#4146,#4147,#4148));
#1121=EDGE_LOOP('',(#4149,#4150,#4151));
#1122=EDGE_LOOP('',(#4152));
#1123=EDGE_LOOP('',(#4153,#4154));
#1124=EDGE_LOOP('',(#4155));
#1125=EDGE_LOOP('',(#4156,#4157,#4158,#4159));
#1126=EDGE_LOOP('',(#4160,#4161));
#1127=EDGE_LOOP('',(#4162));
#1128=EDGE_LOOP('',(#4163,#4164,#4165,#4166));
#1129=EDGE_LOOP('',(#4167,#4168));
#1130=EDGE_LOOP('',(#4169));
#1131=EDGE_LOOP('',(#4170,#4171,#4172,#4173));
#1132=EDGE_LOOP('',(#4174,#4175,#4176,#4177,#4178,#4179,#4180,#4181));
#1133=EDGE_LOOP('',(#4182));
#1134=EDGE_LOOP('',(#4183,#4184,#4185,#4186));
#1135=EDGE_LOOP('',(#4187,#4188,#4189,#4190));
#1136=EDGE_LOOP('',(#4191,#4192,#4193,#4194));
#1137=EDGE_LOOP('',(#4195,#4196,#4197,#4198));
#1138=EDGE_LOOP('',(#4199,#4200,#4201,#4202));
#1139=EDGE_LOOP('',(#4203));
#1140=EDGE_LOOP('',(#4204));
#1141=EDGE_LOOP('',(#4205,#4206,#4207,#4208));
#1142=EDGE_LOOP('',(#4209,#4210,#4211,#4212,#4213,#4214,#4215,#4216,#4217,
#4218,#4219,#4220,#4221,#4222,#4223,#4224,#4225,#4226,#4227,#4228));
#1143=EDGE_LOOP('',(#4229));
#1144=EDGE_LOOP('',(#4230));
#1145=EDGE_LOOP('',(#4231));
#1146=EDGE_LOOP('',(#4232));
#1147=EDGE_LOOP('',(#4233));
#1148=EDGE_LOOP('',(#4234));
#1532=LINE('',#9089,#1906);
#1533=LINE('',#9093,#1907);
#1534=LINE('',#9110,#1908);
#1535=LINE('',#9113,#1909);
#1536=LINE('',#9123,#1910);
#1537=LINE('',#9126,#1911);
#1538=LINE('',#9136,#1912);
#1539=LINE('',#9139,#1913);
#1540=LINE('',#9150,#1914);
#1541=LINE('',#9154,#1915);
#1542=LINE('',#9158,#1916);
#1543=LINE('',#9162,#1917);
#1544=LINE('',#9167,#1918);
#1545=LINE('',#9173,#1919);
#1546=LINE('',#9176,#1920);
#1906=VECTOR('',#7232,1.);
#1907=VECTOR('',#7235,1.);
#1908=VECTOR('',#7256,1.);
#1909=VECTOR('',#7259,1.);
#1910=VECTOR('',#7270,1.);
#1911=VECTOR('',#7273,1.);
#1912=VECTOR('',#7284,1.);
#1913=VECTOR('',#7287,1.);
#1914=VECTOR('',#7304,0.225);
#1915=VECTOR('',#7309,0.225);
#1916=VECTOR('',#7314,0.225);
#1917=VECTOR('',#7319,0.225);
#1918=VECTOR('',#7324,1.49);
#1919=VECTOR('',#7333,0.71);
#1920=VECTOR('',#7336,2.);
#2259=CIRCLE('',#6197,0.375);
#2260=CIRCLE('',#6198,0.375);
#2261=CIRCLE('',#6200,2.);
#2262=CIRCLE('',#6201,2.);
#2263=CIRCLE('',#6202,0.225);
#2264=CIRCLE('',#6204,2.);
#2265=CIRCLE('',#6205,0.375);
#2266=CIRCLE('',#6206,0.225);
#2267=CIRCLE('',#6208,0.375);
#2268=CIRCLE('',#6210,2.);
#2269=CIRCLE('',#6211,0.375);
#2270=CIRCLE('',#6212,0.225);
#2271=CIRCLE('',#6214,0.375);
#2272=CIRCLE('',#6216,2.);
#2273=CIRCLE('',#6217,0.375);
#2274=CIRCLE('',#6218,0.225);
#2275=CIRCLE('',#6220,0.375);
#2276=CIRCLE('',#6222,2.);
#2277=CIRCLE('',#6223,2.);
#2278=CIRCLE('',#6224,2.);
#2279=CIRCLE('',#6225,2.);
#2280=CIRCLE('',#6226,0.71);
#2281=CIRCLE('',#6228,0.225);
#2282=CIRCLE('',#6230,0.225);
#2283=CIRCLE('',#6232,0.225);
#2284=CIRCLE('',#6234,0.225);
#2285=CIRCLE('',#6236,1.49);
#2286=CIRCLE('',#6237,1.49);
#2287=CIRCLE('',#6239,0.71);
#2288=CIRCLE('',#6242,2.);
#2627=VERTEX_POINT('',#9087);
#2628=VERTEX_POINT('',#9088);
#2629=VERTEX_POINT('',#9090);
#2630=VERTEX_POINT('',#9092);
#2631=VERTEX_POINT('',#9096);
#2632=VERTEX_POINT('',#9099);
#2633=VERTEX_POINT('',#9102);
#2634=VERTEX_POINT('',#9103);
#2635=VERTEX_POINT('',#9106);
#2636=VERTEX_POINT('',#9109);
#2637=VERTEX_POINT('',#9111);
#2638=VERTEX_POINT('',#9115);
#2639=VERTEX_POINT('',#9116);
#2640=VERTEX_POINT('',#9119);
#2641=VERTEX_POINT('',#9122);
#2642=VERTEX_POINT('',#9124);
#2643=VERTEX_POINT('',#9128);
#2644=VERTEX_POINT('',#9129);
#2645=VERTEX_POINT('',#9132);
#2646=VERTEX_POINT('',#9135);
#2647=VERTEX_POINT('',#9137);
#2648=VERTEX_POINT('',#9145);
#2649=VERTEX_POINT('',#9148);
#2650=VERTEX_POINT('',#9152);
#2651=VERTEX_POINT('',#9156);
#2652=VERTEX_POINT('',#9160);
#2653=VERTEX_POINT('',#9164);
#2654=VERTEX_POINT('',#9166);
#2655=VERTEX_POINT('',#9170);
#2656=VERTEX_POINT('',#9175);
#3198=EDGE_CURVE('',#2627,#2628,#1532,.T.);
#3199=EDGE_CURVE('',#2629,#2627,#2259,.T.);
#3200=EDGE_CURVE('',#2630,#2629,#1533,.T.);
#3201=EDGE_CURVE('',#2628,#2630,#2260,.T.);
#3202=EDGE_CURVE('',#2629,#2631,#2261,.T.);
#3203=EDGE_CURVE('',#2631,#2627,#2262,.T.);
#3204=EDGE_CURVE('',#2632,#2632,#2263,.T.);
#3205=EDGE_CURVE('',#2633,#2634,#2264,.T.);
#3206=EDGE_CURVE('',#2633,#2634,#2265,.T.);
#3207=EDGE_CURVE('',#2635,#2635,#2266,.T.);
#3208=EDGE_CURVE('',#2636,#2633,#1534,.T.);
#3209=EDGE_CURVE('',#2637,#2636,#2267,.T.);
#3210=EDGE_CURVE('',#2634,#2637,#1535,.T.);
#3211=EDGE_CURVE('',#2638,#2639,#2268,.T.);
#3212=EDGE_CURVE('',#2638,#2639,#2269,.T.);
#3213=EDGE_CURVE('',#2640,#2640,#2270,.T.);
#3214=EDGE_CURVE('',#2641,#2638,#1536,.T.);
#3215=EDGE_CURVE('',#2642,#2641,#2271,.T.);
#3216=EDGE_CURVE('',#2639,#2642,#1537,.T.);
#3217=EDGE_CURVE('',#2643,#2644,#2272,.T.);
#3218=EDGE_CURVE('',#2643,#2644,#2273,.T.);
#3219=EDGE_CURVE('',#2645,#2645,#2274,.T.);
#3220=EDGE_CURVE('',#2646,#2643,#1538,.T.);
#3221=EDGE_CURVE('',#2647,#2646,#2275,.T.);
#3222=EDGE_CURVE('',#2644,#2647,#1539,.T.);
#3223=EDGE_CURVE('',#2630,#2647,#2276,.T.);
#3224=EDGE_CURVE('',#2646,#2642,#2277,.T.);
#3225=EDGE_CURVE('',#2641,#2637,#2278,.T.);
#3226=EDGE_CURVE('',#2636,#2628,#2279,.T.);
#3227=EDGE_CURVE('',#2648,#2648,#2280,.T.);
#3228=EDGE_CURVE('',#2649,#2649,#2281,.T.);
#3229=EDGE_CURVE('',#2649,#2632,#1540,.T.);
#3230=EDGE_CURVE('',#2650,#2650,#2282,.T.);
#3231=EDGE_CURVE('',#2650,#2635,#1541,.T.);
#3232=EDGE_CURVE('',#2651,#2651,#2283,.T.);
#3233=EDGE_CURVE('',#2651,#2640,#1542,.T.);
#3234=EDGE_CURVE('',#2652,#2652,#2284,.T.);
#3235=EDGE_CURVE('',#2652,#2645,#1543,.T.);
#3236=EDGE_CURVE('',#2653,#2653,#2285,.T.);
#3237=EDGE_CURVE('',#2653,#2654,#1544,.T.);
#3238=EDGE_CURVE('',#2654,#2654,#2286,.T.);
#3239=EDGE_CURVE('',#2655,#2655,#2287,.T.);
#3240=EDGE_CURVE('',#2648,#2655,#1545,.T.);
#3241=EDGE_CURVE('',#2631,#2656,#1546,.T.);
#3242=EDGE_CURVE('',#2656,#2656,#2288,.T.);
#4145=ORIENTED_EDGE('',*,*,#3198,.F.);
#4146=ORIENTED_EDGE('',*,*,#3199,.F.);
#4147=ORIENTED_EDGE('',*,*,#3200,.F.);
#4148=ORIENTED_EDGE('',*,*,#3201,.F.);
#4149=ORIENTED_EDGE('',*,*,#3202,.F.);
#4150=ORIENTED_EDGE('',*,*,#3199,.T.);
#4151=ORIENTED_EDGE('',*,*,#3203,.F.);
#4152=ORIENTED_EDGE('',*,*,#3204,.F.);
#4153=ORIENTED_EDGE('',*,*,#3205,.F.);
#4154=ORIENTED_EDGE('',*,*,#3206,.T.);
#4155=ORIENTED_EDGE('',*,*,#3207,.F.);
#4156=ORIENTED_EDGE('',*,*,#3208,.F.);
#4157=ORIENTED_EDGE('',*,*,#3209,.F.);
#4158=ORIENTED_EDGE('',*,*,#3210,.F.);
#4159=ORIENTED_EDGE('',*,*,#3206,.F.);
#4160=ORIENTED_EDGE('',*,*,#3211,.F.);
#4161=ORIENTED_EDGE('',*,*,#3212,.T.);
#4162=ORIENTED_EDGE('',*,*,#3213,.F.);
#4163=ORIENTED_EDGE('',*,*,#3214,.F.);
#4164=ORIENTED_EDGE('',*,*,#3215,.F.);
#4165=ORIENTED_EDGE('',*,*,#3216,.F.);
#4166=ORIENTED_EDGE('',*,*,#3212,.F.);
#4167=ORIENTED_EDGE('',*,*,#3217,.F.);
#4168=ORIENTED_EDGE('',*,*,#3218,.T.);
#4169=ORIENTED_EDGE('',*,*,#3219,.F.);
#4170=ORIENTED_EDGE('',*,*,#3220,.F.);
#4171=ORIENTED_EDGE('',*,*,#3221,.F.);
#4172=ORIENTED_EDGE('',*,*,#3222,.F.);
#4173=ORIENTED_EDGE('',*,*,#3218,.F.);
#4174=ORIENTED_EDGE('',*,*,#3201,.T.);
#4175=ORIENTED_EDGE('',*,*,#3223,.T.);
#4176=ORIENTED_EDGE('',*,*,#3221,.T.);
#4177=ORIENTED_EDGE('',*,*,#3224,.T.);
#4178=ORIENTED_EDGE('',*,*,#3215,.T.);
#4179=ORIENTED_EDGE('',*,*,#3225,.T.);
#4180=ORIENTED_EDGE('',*,*,#3209,.T.);
#4181=ORIENTED_EDGE('',*,*,#3226,.T.);
#4182=ORIENTED_EDGE('',*,*,#3227,.T.);
#4183=ORIENTED_EDGE('',*,*,#3228,.F.);
#4184=ORIENTED_EDGE('',*,*,#3229,.T.);
#4185=ORIENTED_EDGE('',*,*,#3204,.T.);
#4186=ORIENTED_EDGE('',*,*,#3229,.F.);
#4187=ORIENTED_EDGE('',*,*,#3230,.F.);
#4188=ORIENTED_EDGE('',*,*,#3231,.T.);
#4189=ORIENTED_EDGE('',*,*,#3207,.T.);
#4190=ORIENTED_EDGE('',*,*,#3231,.F.);
#4191=ORIENTED_EDGE('',*,*,#3232,.F.);
#4192=ORIENTED_EDGE('',*,*,#3233,.T.);
#4193=ORIENTED_EDGE('',*,*,#3213,.T.);
#4194=ORIENTED_EDGE('',*,*,#3233,.F.);
#4195=ORIENTED_EDGE('',*,*,#3234,.F.);
#4196=ORIENTED_EDGE('',*,*,#3235,.T.);
#4197=ORIENTED_EDGE('',*,*,#3219,.T.);
#4198=ORIENTED_EDGE('',*,*,#3235,.F.);
#4199=ORIENTED_EDGE('',*,*,#3236,.F.);
#4200=ORIENTED_EDGE('',*,*,#3237,.T.);
#4201=ORIENTED_EDGE('',*,*,#3238,.T.);
#4202=ORIENTED_EDGE('',*,*,#3237,.F.);
#4203=ORIENTED_EDGE('',*,*,#3238,.F.);
#4204=ORIENTED_EDGE('',*,*,#3239,.F.);
#4205=ORIENTED_EDGE('',*,*,#3227,.F.);
#4206=ORIENTED_EDGE('',*,*,#3240,.T.);
#4207=ORIENTED_EDGE('',*,*,#3239,.T.);
#4208=ORIENTED_EDGE('',*,*,#3240,.F.);
#4209=ORIENTED_EDGE('',*,*,#3198,.T.);
#4210=ORIENTED_EDGE('',*,*,#3226,.F.);
#4211=ORIENTED_EDGE('',*,*,#3208,.T.);
#4212=ORIENTED_EDGE('',*,*,#3205,.T.);
#4213=ORIENTED_EDGE('',*,*,#3210,.T.);
#4214=ORIENTED_EDGE('',*,*,#3225,.F.);
#4215=ORIENTED_EDGE('',*,*,#3214,.T.);
#4216=ORIENTED_EDGE('',*,*,#3211,.T.);
#4217=ORIENTED_EDGE('',*,*,#3216,.T.);
#4218=ORIENTED_EDGE('',*,*,#3224,.F.);
#4219=ORIENTED_EDGE('',*,*,#3220,.T.);
#4220=ORIENTED_EDGE('',*,*,#3217,.T.);
#4221=ORIENTED_EDGE('',*,*,#3222,.T.);
#4222=ORIENTED_EDGE('',*,*,#3223,.F.);
#4223=ORIENTED_EDGE('',*,*,#3200,.T.);
#4224=ORIENTED_EDGE('',*,*,#3202,.T.);
#4225=ORIENTED_EDGE('',*,*,#3241,.T.);
#4226=ORIENTED_EDGE('',*,*,#3242,.T.);
#4227=ORIENTED_EDGE('',*,*,#3241,.F.);
#4228=ORIENTED_EDGE('',*,*,#3203,.T.);
#4229=ORIENTED_EDGE('',*,*,#3242,.F.);
#4230=ORIENTED_EDGE('',*,*,#3236,.T.);
#4231=ORIENTED_EDGE('',*,*,#3234,.T.);
#4232=ORIENTED_EDGE('',*,*,#3232,.T.);
#4233=ORIENTED_EDGE('',*,*,#3230,.T.);
#4234=ORIENTED_EDGE('',*,*,#3228,.T.);
#5284=CYLINDRICAL_SURFACE('',#6196,0.375);
#5285=CYLINDRICAL_SURFACE('',#6207,0.375);
#5286=CYLINDRICAL_SURFACE('',#6213,0.375);
#5287=CYLINDRICAL_SURFACE('',#6219,0.375);
#5288=CYLINDRICAL_SURFACE('',#6227,0.225);
#5289=CYLINDRICAL_SURFACE('',#6229,0.225);
#5290=CYLINDRICAL_SURFACE('',#6231,0.225);
#5291=CYLINDRICAL_SURFACE('',#6233,0.225);
#5292=CYLINDRICAL_SURFACE('',#6235,1.49);
#5293=CYLINDRICAL_SURFACE('',#6240,0.71);
#5294=CYLINDRICAL_SURFACE('',#6241,2.);
#5456=ADVANCED_FACE('',(#742),#5284,.F.);
#5457=ADVANCED_FACE('',(#743,#412),#521,.T.);
#5458=ADVANCED_FACE('',(#744,#413),#522,.T.);
#5459=ADVANCED_FACE('',(#745),#5285,.F.);
#5460=ADVANCED_FACE('',(#746,#414),#523,.T.);
#5461=ADVANCED_FACE('',(#747),#5286,.F.);
#5462=ADVANCED_FACE('',(#748,#415),#524,.T.);
#5463=ADVANCED_FACE('',(#749),#5287,.F.);
#5464=ADVANCED_FACE('',(#750,#416),#525,.T.);
#5465=ADVANCED_FACE('',(#751),#5288,.F.);
#5466=ADVANCED_FACE('',(#752),#5289,.F.);
#5467=ADVANCED_FACE('',(#753),#5290,.F.);
#5468=ADVANCED_FACE('',(#754),#5291,.F.);
#5469=ADVANCED_FACE('',(#755),#5292,.T.);
#5470=ADVANCED_FACE('',(#756,#417),#526,.F.);
#5471=ADVANCED_FACE('',(#757),#5293,.F.);
#5472=ADVANCED_FACE('',(#758),#5294,.T.);
#5473=ADVANCED_FACE('',(#759,#418,#419,#420,#421,#422),#527,.F.);
#5704=CLOSED_SHELL('',(#5456,#5457,#5458,#5459,#5460,#5461,#5462,#5463,
#5464,#5465,#5466,#5467,#5468,#5469,#5470,#5471,#5472,#5473));
#6195=AXIS2_PLACEMENT_3D('',#9085,#7228,#7229);
#6196=AXIS2_PLACEMENT_3D('',#9086,#7230,#7231);
#6197=AXIS2_PLACEMENT_3D('',#9091,#7233,#7234);
#6198=AXIS2_PLACEMENT_3D('',#9094,#7236,#7237);
#6199=AXIS2_PLACEMENT_3D('',#9095,#7238,#7239);
#6200=AXIS2_PLACEMENT_3D('',#9097,#7240,#7241);
#6201=AXIS2_PLACEMENT_3D('',#9098,#7242,#7243);
#6202=AXIS2_PLACEMENT_3D('',#9100,#7244,#7245);
#6203=AXIS2_PLACEMENT_3D('',#9101,#7246,#7247);
#6204=AXIS2_PLACEMENT_3D('',#9104,#7248,#7249);
#6205=AXIS2_PLACEMENT_3D('',#9105,#7250,#7251);
#6206=AXIS2_PLACEMENT_3D('',#9107,#7252,#7253);
#6207=AXIS2_PLACEMENT_3D('',#9108,#7254,#7255);
#6208=AXIS2_PLACEMENT_3D('',#9112,#7257,#7258);
#6209=AXIS2_PLACEMENT_3D('',#9114,#7260,#7261);
#6210=AXIS2_PLACEMENT_3D('',#9117,#7262,#7263);
#6211=AXIS2_PLACEMENT_3D('',#9118,#7264,#7265);
#6212=AXIS2_PLACEMENT_3D('',#9120,#7266,#7267);
#6213=AXIS2_PLACEMENT_3D('',#9121,#7268,#7269);
#6214=AXIS2_PLACEMENT_3D('',#9125,#7271,#7272);
#6215=AXIS2_PLACEMENT_3D('',#9127,#7274,#7275);
#6216=AXIS2_PLACEMENT_3D('',#9130,#7276,#7277);
#6217=AXIS2_PLACEMENT_3D('',#9131,#7278,#7279);
#6218=AXIS2_PLACEMENT_3D('',#9133,#7280,#7281);
#6219=AXIS2_PLACEMENT_3D('',#9134,#7282,#7283);
#6220=AXIS2_PLACEMENT_3D('',#9138,#7285,#7286);
#6221=AXIS2_PLACEMENT_3D('',#9140,#7288,#7289);
#6222=AXIS2_PLACEMENT_3D('',#9141,#7290,#7291);
#6223=AXIS2_PLACEMENT_3D('',#9142,#7292,#7293);
#6224=AXIS2_PLACEMENT_3D('',#9143,#7294,#7295);
#6225=AXIS2_PLACEMENT_3D('',#9144,#7296,#7297);
#6226=AXIS2_PLACEMENT_3D('',#9146,#7298,#7299);
#6227=AXIS2_PLACEMENT_3D('',#9147,#7300,#7301);
#6228=AXIS2_PLACEMENT_3D('',#9149,#7302,#7303);
#6229=AXIS2_PLACEMENT_3D('',#9151,#7305,#7306);
#6230=AXIS2_PLACEMENT_3D('',#9153,#7307,#7308);
#6231=AXIS2_PLACEMENT_3D('',#9155,#7310,#7311);
#6232=AXIS2_PLACEMENT_3D('',#9157,#7312,#7313);
#6233=AXIS2_PLACEMENT_3D('',#9159,#7315,#7316);
#6234=AXIS2_PLACEMENT_3D('',#9161,#7317,#7318);
#6235=AXIS2_PLACEMENT_3D('',#9163,#7320,#7321);
#6236=AXIS2_PLACEMENT_3D('',#9165,#7322,#7323);
#6237=AXIS2_PLACEMENT_3D('',#9168,#7325,#7326);
#6238=AXIS2_PLACEMENT_3D('',#9169,#7327,#7328);
#6239=AXIS2_PLACEMENT_3D('',#9171,#7329,#7330);
#6240=AXIS2_PLACEMENT_3D('',#9172,#7331,#7332);
#6241=AXIS2_PLACEMENT_3D('',#9174,#7334,#7335);
#6242=AXIS2_PLACEMENT_3D('',#9177,#7337,#7338);
#6243=AXIS2_PLACEMENT_3D('',#9178,#7339,#7340);
#7228=DIRECTION('axis',(0.,0.,1.));
#7229=DIRECTION('refdir',(1.,0.,0.));
#7230=DIRECTION('center_axis',(0.,0.,1.));
#7231=DIRECTION('ref_axis',(1.,0.,0.));
#7232=DIRECTION('',(0.,0.,1.));
#7233=DIRECTION('center_axis',(0.,0.,1.));
#7234=DIRECTION('ref_axis',(1.,0.,0.));
#7235=DIRECTION('',(0.,0.,-1.));
#7236=DIRECTION('center_axis',(0.,0.,-1.));
#7237=DIRECTION('ref_axis',(1.,0.,0.));
#7238=DIRECTION('center_axis',(0.,0.,1.));
#7239=DIRECTION('ref_axis',(1.,0.,0.));
#7240=DIRECTION('center_axis',(0.,0.,-1.));
#7241=DIRECTION('ref_axis',(1.,0.,0.));
#7242=DIRECTION('center_axis',(0.,0.,-1.));
#7243=DIRECTION('ref_axis',(1.,0.,0.));
#7244=DIRECTION('center_axis',(0.,0.,1.));
#7245=DIRECTION('ref_axis',(1.,0.,0.));
#7246=DIRECTION('center_axis',(0.,0.,1.));
#7247=DIRECTION('ref_axis',(1.,0.,0.));
#7248=DIRECTION('center_axis',(0.,0.,-1.));
#7249=DIRECTION('ref_axis',(1.,0.,0.));
#7250=DIRECTION('center_axis',(0.,0.,1.));
#7251=DIRECTION('ref_axis',(1.,0.,0.));
#7252=DIRECTION('center_axis',(0.,0.,1.));
#7253=DIRECTION('ref_axis',(1.,0.,0.));
#7254=DIRECTION('center_axis',(0.,0.,1.));
#7255=DIRECTION('ref_axis',(-1.83697019872103E-16,-1.,0.));
#7256=DIRECTION('',(0.,0.,-1.));
#7257=DIRECTION('center_axis',(0.,0.,-1.));
#7258=DIRECTION('ref_axis',(1.,0.,0.));
#7259=DIRECTION('',(0.,0.,1.));
#7260=DIRECTION('center_axis',(0.,0.,1.));
#7261=DIRECTION('ref_axis',(1.,0.,0.));
#7262=DIRECTION('center_axis',(0.,0.,-1.));
#7263=DIRECTION('ref_axis',(1.,0.,0.));
#7264=DIRECTION('center_axis',(0.,0.,1.));
#7265=DIRECTION('ref_axis',(1.,0.,0.));
#7266=DIRECTION('center_axis',(0.,0.,1.));
#7267=DIRECTION('ref_axis',(1.,0.,0.));
#7268=DIRECTION('center_axis',(0.,0.,1.));
#7269=DIRECTION('ref_axis',(-1.,1.22464679914735E-16,0.));
#7270=DIRECTION('',(0.,0.,-1.));
#7271=DIRECTION('center_axis',(0.,0.,-1.));
#7272=DIRECTION('ref_axis',(1.,0.,0.));
#7273=DIRECTION('',(0.,0.,1.));
#7274=DIRECTION('center_axis',(0.,0.,1.));
#7275=DIRECTION('ref_axis',(1.,0.,0.));
#7276=DIRECTION('center_axis',(0.,0.,-1.));
#7277=DIRECTION('ref_axis',(1.,0.,0.));
#7278=DIRECTION('center_axis',(0.,0.,1.));
#7279=DIRECTION('ref_axis',(1.,0.,0.));
#7280=DIRECTION('center_axis',(0.,0.,1.));
#7281=DIRECTION('ref_axis',(1.,0.,0.));
#7282=DIRECTION('center_axis',(0.,0.,1.));
#7283=DIRECTION('ref_axis',(-6.04901474817726E-16,1.,0.));
#7284=DIRECTION('',(0.,0.,-1.));
#7285=DIRECTION('center_axis',(0.,0.,-1.));
#7286=DIRECTION('ref_axis',(1.,0.,0.));
#7287=DIRECTION('',(0.,0.,1.));
#7288=DIRECTION('center_axis',(0.,0.,1.));
#7289=DIRECTION('ref_axis',(1.,0.,0.));
#7290=DIRECTION('center_axis',(0.,0.,1.));
#7291=DIRECTION('ref_axis',(1.,0.,0.));
#7292=DIRECTION('center_axis',(0.,0.,1.));
#7293=DIRECTION('ref_axis',(1.,0.,0.));
#7294=DIRECTION('center_axis',(0.,0.,1.));
#7295=DIRECTION('ref_axis',(1.,0.,0.));
#7296=DIRECTION('center_axis',(0.,0.,1.));
#7297=DIRECTION('ref_axis',(1.,0.,0.));
#7298=DIRECTION('center_axis',(0.,0.,-1.));
#7299=DIRECTION('ref_axis',(1.,0.,0.));
#7300=DIRECTION('center_axis',(0.,0.,1.));
#7301=DIRECTION('ref_axis',(1.,0.,0.));
#7302=DIRECTION('center_axis',(0.,0.,1.));
#7303=DIRECTION('ref_axis',(1.,0.,0.));
#7304=DIRECTION('',(0.,0.,1.));
#7305=DIRECTION('center_axis',(0.,0.,1.));
#7306=DIRECTION('ref_axis',(1.,0.,0.));
#7307=DIRECTION('center_axis',(0.,0.,1.));
#7308=DIRECTION('ref_axis',(1.,0.,0.));
#7309=DIRECTION('',(0.,0.,1.));
#7310=DIRECTION('center_axis',(0.,0.,1.));
#7311=DIRECTION('ref_axis',(1.,0.,0.));
#7312=DIRECTION('center_axis',(0.,0.,1.));
#7313=DIRECTION('ref_axis',(1.,0.,0.));
#7314=DIRECTION('',(0.,0.,1.));
#7315=DIRECTION('center_axis',(0.,0.,1.));
#7316=DIRECTION('ref_axis',(1.,0.,0.));
#7317=DIRECTION('center_axis',(0.,0.,1.));
#7318=DIRECTION('ref_axis',(1.,0.,0.));
#7319=DIRECTION('',(0.,0.,1.));
#7320=DIRECTION('center_axis',(0.,0.,1.));
#7321=DIRECTION('ref_axis',(1.,0.,0.));
#7322=DIRECTION('center_axis',(0.,0.,1.));
#7323=DIRECTION('ref_axis',(1.,0.,0.));
#7324=DIRECTION('',(0.,0.,-1.));
#7325=DIRECTION('center_axis',(0.,0.,1.));
#7326=DIRECTION('ref_axis',(1.,0.,0.));
#7327=DIRECTION('center_axis',(0.,0.,1.));
#7328=DIRECTION('ref_axis',(1.,0.,0.));
#7329=DIRECTION('center_axis',(0.,0.,-1.));
#7330=DIRECTION('ref_axis',(1.,0.,0.));
#7331=DIRECTION('center_axis',(0.,0.,1.));
#7332=DIRECTION('ref_axis',(1.,0.,0.));
#7333=DIRECTION('',(0.,0.,-1.));
#7334=DIRECTION('center_axis',(0.,0.,1.));
#7335=DIRECTION('ref_axis',(1.,0.,0.));
#7336=DIRECTION('',(0.,0.,-1.));
#7337=DIRECTION('center_axis',(0.,0.,1.));
#7338=DIRECTION('ref_axis',(1.,0.,0.));
#7339=DIRECTION('center_axis',(0.,0.,1.));
#7340=DIRECTION('ref_axis',(1.,0.,0.));
#9085=CARTESIAN_POINT('',(0.,0.,0.));
#9086=CARTESIAN_POINT('Origin',(2.52264068711929,2.10639249453345E-16,4.));
#9087=CARTESIAN_POINT('',(2.26072934990998,0.268379305165721,4.));
#9088=CARTESIAN_POINT('',(2.26072934990998,0.268379305165722,4.4));
#9089=CARTESIAN_POINT('',(2.26072934990998,0.268379305165721,4.));
#9090=CARTESIAN_POINT('',(2.26072934990998,-0.268379305165721,4.));
#9091=CARTESIAN_POINT('Origin',(2.52264068711929,2.10639249453345E-16,4.));
#9092=CARTESIAN_POINT('',(2.26072934990998,-0.268379305165721,4.4));
#9093=CARTESIAN_POINT('',(2.26072934990998,-0.268379305165721,4.));
#9094=CARTESIAN_POINT('Origin',(2.52264068711929,2.10639249453345E-16,4.4));
#9095=CARTESIAN_POINT('Origin',(2.52264068711929,2.22044604925031E-16,4.));
#9096=CARTESIAN_POINT('',(2.24264068711929,-2.44929359829471E-16,4.));
#9097=CARTESIAN_POINT('Origin',(4.24264068711929,0.,4.));
#9098=CARTESIAN_POINT('Origin',(4.24264068711929,0.,4.));
#9099=CARTESIAN_POINT('',(2.29764068711929,1.83084696472529E-16,4.));
#9100=CARTESIAN_POINT('Origin',(2.52264068711929,2.10639249453345E-16,4.));
#9101=CARTESIAN_POINT('Origin',(4.24264068711929,1.72,4.));
#9102=CARTESIAN_POINT('',(3.97426138195357,1.9819113372093,4.));
#9103=CARTESIAN_POINT('',(4.51101999228501,1.9819113372093,4.));
#9104=CARTESIAN_POINT('Origin',(4.24264068711929,0.,4.));
#9105=CARTESIAN_POINT('Origin',(4.24264068711929,1.72,4.));
#9106=CARTESIAN_POINT('',(4.01764068711929,1.72,4.));
#9107=CARTESIAN_POINT('Origin',(4.24264068711929,1.72,4.));
#9108=CARTESIAN_POINT('Origin',(4.24264068711929,1.72,4.));
#9109=CARTESIAN_POINT('',(3.97426138195357,1.9819113372093,4.4));
#9110=CARTESIAN_POINT('',(3.97426138195357,1.9819113372093,4.));
#9111=CARTESIAN_POINT('',(4.51101999228501,1.9819113372093,4.4));
#9112=CARTESIAN_POINT('Origin',(4.24264068711929,1.72,4.4));
#9113=CARTESIAN_POINT('',(4.51101999228501,1.9819113372093,4.));
#9114=CARTESIAN_POINT('Origin',(5.96264068711929,0.,4.));
#9115=CARTESIAN_POINT('',(6.22455202432859,0.268379305165721,4.));
#9116=CARTESIAN_POINT('',(6.22455202432859,-0.268379305165721,4.));
#9117=CARTESIAN_POINT('Origin',(4.24264068711929,0.,4.));
#9118=CARTESIAN_POINT('Origin',(5.96264068711929,0.,4.));
#9119=CARTESIAN_POINT('',(5.73764068711929,-2.75545529808154E-17,4.));
#9120=CARTESIAN_POINT('Origin',(5.96264068711929,0.,4.));
#9121=CARTESIAN_POINT('Origin',(5.96264068711929,0.,4.));
#9122=CARTESIAN_POINT('',(6.22455202432859,0.26837930516572,4.4));
#9123=CARTESIAN_POINT('',(6.22455202432859,0.268379305165721,4.));
#9124=CARTESIAN_POINT('',(6.22455202432859,-0.26837930516572,4.4));
#9125=CARTESIAN_POINT('Origin',(5.96264068711929,0.,4.4));
#9126=CARTESIAN_POINT('',(6.22455202432859,-0.268379305165721,4.));
#9127=CARTESIAN_POINT('Origin',(4.24264068711929,-1.72,4.));
#9128=CARTESIAN_POINT('',(4.51101999228501,-1.9819113372093,4.));
#9129=CARTESIAN_POINT('',(3.97426138195357,-1.9819113372093,4.));
#9130=CARTESIAN_POINT('Origin',(4.24264068711929,0.,4.));
#9131=CARTESIAN_POINT('Origin',(4.24264068711929,-1.72,4.));
#9132=CARTESIAN_POINT('',(4.01764068711929,-1.72,4.));
#9133=CARTESIAN_POINT('Origin',(4.24264068711929,-1.72,4.));
#9134=CARTESIAN_POINT('Origin',(4.24264068711929,-1.72,4.));
#9135=CARTESIAN_POINT('',(4.51101999228501,-1.9819113372093,4.4));
#9136=CARTESIAN_POINT('',(4.51101999228501,-1.9819113372093,4.));
#9137=CARTESIAN_POINT('',(3.97426138195357,-1.9819113372093,4.4));
#9138=CARTESIAN_POINT('Origin',(4.24264068711929,-1.72,4.4));
#9139=CARTESIAN_POINT('',(3.97426138195357,-1.9819113372093,4.));
#9140=CARTESIAN_POINT('Origin',(4.24264068711929,0.,4.4));
#9141=CARTESIAN_POINT('Origin',(4.24264068711929,0.,4.4));
#9142=CARTESIAN_POINT('Origin',(4.24264068711929,0.,4.4));
#9143=CARTESIAN_POINT('Origin',(4.24264068711929,0.,4.4));
#9144=CARTESIAN_POINT('Origin',(4.24264068711929,0.,4.4));
#9145=CARTESIAN_POINT('',(3.53264068711929,-8.69499227394621E-17,4.4));
#9146=CARTESIAN_POINT('Origin',(4.24264068711929,0.,4.4));
#9147=CARTESIAN_POINT('Origin',(2.52264068711929,2.10639249453345E-16,3.5));
#9148=CARTESIAN_POINT('',(2.29764068711929,1.83084696472529E-16,3.6));
#9149=CARTESIAN_POINT('Origin',(2.52264068711929,2.10639249453345E-16,3.6));
#9150=CARTESIAN_POINT('',(2.29764068711929,1.83084696472529E-16,3.5));
#9151=CARTESIAN_POINT('Origin',(4.24264068711929,1.72,3.5));
#9152=CARTESIAN_POINT('',(4.01764068711929,1.72,3.6));
#9153=CARTESIAN_POINT('Origin',(4.24264068711929,1.72,3.6));
#9154=CARTESIAN_POINT('',(4.01764068711929,1.72,3.5));
#9155=CARTESIAN_POINT('Origin',(5.96264068711929,0.,3.5));
#9156=CARTESIAN_POINT('',(5.73764068711929,-2.75545529808154E-17,3.6));
#9157=CARTESIAN_POINT('Origin',(5.96264068711929,0.,3.6));
#9158=CARTESIAN_POINT('',(5.73764068711929,-2.75545529808154E-17,3.5));
#9159=CARTESIAN_POINT('Origin',(4.24264068711929,-1.72,3.5));
#9160=CARTESIAN_POINT('',(4.01764068711929,-1.72,3.6));
#9161=CARTESIAN_POINT('Origin',(4.24264068711929,-1.72,3.6));
#9162=CARTESIAN_POINT('',(4.01764068711929,-1.72,3.5));
#9163=CARTESIAN_POINT('Origin',(4.24264068711929,0.,2.95));
#9164=CARTESIAN_POINT('',(2.75264068711929,-1.82472373072956E-16,3.6));
#9165=CARTESIAN_POINT('Origin',(4.24264068711929,0.,3.6));
#9166=CARTESIAN_POINT('',(2.75264068711929,-1.82472373072956E-16,2.95));
#9167=CARTESIAN_POINT('',(2.75264068711929,-1.82472373072956E-16,2.95));
#9168=CARTESIAN_POINT('Origin',(4.24264068711929,0.,2.95));
#9169=CARTESIAN_POINT('Origin',(4.24264068711929,0.,2.95));
#9170=CARTESIAN_POINT('',(3.53264068711929,-8.69499227394621E-17,2.95));
#9171=CARTESIAN_POINT('Origin',(4.24264068711929,0.,2.95));
#9172=CARTESIAN_POINT('Origin',(4.24264068711929,0.,3.6));
#9173=CARTESIAN_POINT('',(3.53264068711929,-8.69499227394621E-17,3.6));
#9174=CARTESIAN_POINT('Origin',(4.24264068711929,0.,3.6));
#9175=CARTESIAN_POINT('',(2.24264068711929,-2.44929359829471E-16,3.6));
#9176=CARTESIAN_POINT('',(2.24264068711929,-2.44929359829471E-16,3.6));
#9177=CARTESIAN_POINT('Origin',(4.24264068711929,0.,3.6));
#9178=CARTESIAN_POINT('Origin',(4.24264068711929,0.,3.6));
#10903=UNCERTAINTY_MEASURE_WITH_UNIT(LENGTH_MEASURE(0.001),#10958,
'DISTANCE_ACCURACY_VALUE',
'Maximum model space distance between geometric entities at asserted c
onnectivities');
#10926=UNCERTAINTY_MEASURE_WITH_UNIT(LENGTH_MEASURE(0.001),#10958,
'DISTANCE_ACCURACY_VALUE',
'Maximum model space distance between geometric entities at asserted c
onnectivities');
#10934=(
GEOMETRIC_REPRESENTATION_CONTEXT(3)
GLOBAL_UNCERTAINTY_ASSIGNED_CONTEXT((#10903))
GLOBAL_UNIT_ASSIGNED_CONTEXT((#10958,#10960,#10961))
REPRESENTATION_CONTEXT('','3D')
);
#10957=(
GEOMETRIC_REPRESENTATION_CONTEXT(3)
GLOBAL_UNCERTAINTY_ASSIGNED_CONTEXT((#10926))
GLOBAL_UNIT_ASSIGNED_CONTEXT((#10958,#10960,#10961))
REPRESENTATION_CONTEXT('','3D')
);
#10958=(
LENGTH_UNIT()
NAMED_UNIT(*)
SI_UNIT(.CENTI.,.METRE.)
);
#10960=(
NAMED_UNIT(*)
PLANE_ANGLE_UNIT()
SI_UNIT($,.RADIAN.)
);
#10961=(
NAMED_UNIT(*)
SI_UNIT($,.STERADIAN.)
SOLID_ANGLE_UNIT()
);
#10969=SHAPE_DEFINITION_REPRESENTATION(#10999,#11071);
#10999=PRODUCT_DEFINITION_SHAPE('',$,#11102);
#11071=SHAPE_REPRESENTATION('',(#6195),#10934);
#11094=PRODUCT_DEFINITION_CONTEXT('part definition',#11186,'design');
#11102=PRODUCT_DEFINITION('Bearing cap (1)','Bearing cap (1)',#11132,#11094);
#11132=PRODUCT_DEFINITION_FORMATION('',$,#11195);
#11186=APPLICATION_CONTEXT(
'Core Data for Automotive Mechanical Design Process');
#11187=PRODUCT_CONTEXT('part definition',#11186,'mechanical');
#11195=PRODUCT('Bearing cap (1)','Bearing cap (1)','Bearing cap (1)',(#11187));
#11281=COLOUR_RGB('Grey',0.48,0.52,0.57);
#11282=FILL_AREA_STYLE_COLOUR('',#11281);
#11283=FILL_AREA_STYLE('',(#11282));
#11284=SURFACE_STYLE_FILL_AREA(#11283);
#11285=SURFACE_SIDE_STYLE('',(#11284));
#11286=SURFACE_STYLE_USAGE(.BOTH.,#11285);
#11287=PRESENTATION_STYLE_ASSIGNMENT((#11286));
ENDSEC;
END-ISO-10303-21;
